ISO-10303-21;
HEADER;
FILE_DESCRIPTION((''),'2;1');
FILE_NAME('RETAINER_SCREW_M3x8.step','2026-10-01T22:07:29-07:00',(''),(''),'','','');
FILE_SCHEMA (('AUTOMOTIVE_DESIGN { 1 0 10303 214 3 1 1 }'));
ENDSEC;
DATA;
#10=MECHANICAL_DESIGN_GEOMETRIC_PRESENTATION_REPRESENTATION('',(#583),#15484);
#506=SHAPE_REPRESENTATION_RELATIONSHIP('SRR','None',#15658,#541) ;
#541=ADVANCED_BREP_SHAPE_REPRESENTATION('',(#624),#15482) ;
#583=STYLED_ITEM('',(#15832),#624) ;
#624=MANIFOLD_SOLID_BREP('RETAINER_SCREW_M3x8',#8294) ;
#806=CYLINDRICAL_SURFACE('',#9896,0.15) ;
#807=CYLINDRICAL_SURFACE('',#9900,0.275) ;
#883=FACE_BOUND('',#2433,.T.) ;
#1357=CIRCLE('',#9897,0.15) ;
#1358=CIRCLE('',#9898,0.15) ;
#1359=CIRCLE('',#9901,0.275) ;
#1360=CIRCLE('',#9902,0.275) ;
#1855=FACE_OUTER_BOUND('',#2428,.T.) ;
#1856=FACE_OUTER_BOUND('',#2429,.T.) ;
#1857=FACE_OUTER_BOUND('',#2430,.T.) ;
#1858=FACE_OUTER_BOUND('',#2431,.T.) ;
#1859=FACE_OUTER_BOUND('',#2432,.T.) ;
#2428=EDGE_LOOP('',(#7513,#7514,#7515,#7516)) ;
#2429=EDGE_LOOP('',(#7517)) ;
#2430=EDGE_LOOP('',(#7518,#7519,#7520,#7521)) ;
#2431=EDGE_LOOP('',(#7522)) ;
#2432=EDGE_LOOP('',(#7523)) ;
#2433=EDGE_LOOP('',(#7524)) ;
#2910=LINE('',#15362,#3384) ;
#2911=LINE('',#15369,#3385) ;
#3384=VECTOR('',#12827,0.15) ;
#3385=VECTOR('',#12836,0.275) ;
#4133=VERTEX_POINT('',#15359) ;
#4134=VERTEX_POINT('',#15361) ;
#4135=VERTEX_POINT('',#15366) ;
#4136=VERTEX_POINT('',#15368) ;
#5261=EDGE_CURVE('',#4133,#4133,#1357,.T.) ;
#5262=EDGE_CURVE('',#4133,#4134,#2910,.T.) ;
#5263=EDGE_CURVE('',#4134,#4134,#1358,.T.) ;
#5264=EDGE_CURVE('',#4135,#4135,#1359,.T.) ;
#5265=EDGE_CURVE('',#4135,#4136,#2911,.T.) ;
#5266=EDGE_CURVE('',#4136,#4136,#1360,.T.) ;
#7513=ORIENTED_EDGE('',*,*,#5261,.F.) ;
#7514=ORIENTED_EDGE('',*,*,#5262,.T.) ;
#7515=ORIENTED_EDGE('',*,*,#5263,.F.) ;
#7516=ORIENTED_EDGE('',*,*,#5262,.F.) ;
#7517=ORIENTED_EDGE('',*,*,#5261,.T.) ;
#7518=ORIENTED_EDGE('',*,*,#5264,.F.) ;
#7519=ORIENTED_EDGE('',*,*,#5265,.T.) ;
#7520=ORIENTED_EDGE('',*,*,#5266,.F.) ;
#7521=ORIENTED_EDGE('',*,*,#5265,.F.) ;
#7522=ORIENTED_EDGE('',*,*,#5266,.T.) ;
#7523=ORIENTED_EDGE('',*,*,#5264,.T.) ;
#7524=ORIENTED_EDGE('',*,*,#5263,.T.) ;
#7746=PLANE('',#9899) ;
#7747=PLANE('',#9903) ;
#7748=PLANE('',#9904) ;
#8242=ADVANCED_FACE('',(#1855),#806,.T.) ;
#8243=ADVANCED_FACE('',(#1856),#7746,.T.) ;
#8244=ADVANCED_FACE('',(#1857),#807,.T.) ;
#8245=ADVANCED_FACE('',(#1858),#7747,.T.) ;
#8246=ADVANCED_FACE('',(#1859,#883),#7748,.T.) ;
#8294=CLOSED_SHELL('',(#8242,#8243,#8244,#8245,#8246)) ;
#9895=AXIS2_PLACEMENT_3D('',#15357,#12821,#12822) ;
#9896=AXIS2_PLACEMENT_3D('',#15358,#12823,#12824) ;
#9897=AXIS2_PLACEMENT_3D('',#15360,#12825,#12826) ;
#9898=AXIS2_PLACEMENT_3D('',#15363,#12828,#12829) ;
#9899=AXIS2_PLACEMENT_3D('',#15364,#12830,#12831) ;
#9900=AXIS2_PLACEMENT_3D('',#15365,#12832,#12833) ;
#9901=AXIS2_PLACEMENT_3D('',#15367,#12834,#12835) ;
#9902=AXIS2_PLACEMENT_3D('',#15370,#12837,#12838) ;
#9903=AXIS2_PLACEMENT_3D('',#15371,#12839,#12840) ;
#9904=AXIS2_PLACEMENT_3D('',#15372,#12841,#12842) ;
#12821=DIRECTION('axis',(0.,0.,1.)) ;
#12822=DIRECTION('refdir',(1.,0.,0.)) ;
#12823=DIRECTION('center_axis',(0.,0.,1.)) ;
#12824=DIRECTION('ref_axis',(1.,0.,0.)) ;
#12825=DIRECTION('center_axis',(0.,0.,1.)) ;
#12826=DIRECTION('ref_axis',(1.,0.,0.)) ;
#12827=DIRECTION('',(0.,0.,-1.)) ;
#12828=DIRECTION('center_axis',(0.,0.,-1.)) ;
#12829=DIRECTION('ref_axis',(1.,0.,0.)) ;
#12830=DIRECTION('center_axis',(0.,0.,1.)) ;
#12831=DIRECTION('ref_axis',(1.,0.,0.)) ;
#12832=DIRECTION('center_axis',(0.,0.,1.)) ;
#12833=DIRECTION('ref_axis',(1.,0.,0.)) ;
#12834=DIRECTION('center_axis',(0.,0.,1.)) ;
#12835=DIRECTION('ref_axis',(1.,0.,0.)) ;
#12836=DIRECTION('',(0.,0.,-1.)) ;
#12837=DIRECTION('center_axis',(0.,0.,-1.)) ;
#12838=DIRECTION('ref_axis',(1.,0.,0.)) ;
#12839=DIRECTION('center_axis',(0.,0.,-1.)) ;
#12840=DIRECTION('ref_axis',(-1.,0.,0.)) ;
#12841=DIRECTION('center_axis',(0.,0.,1.)) ;
#12842=DIRECTION('ref_axis',(1.,0.,0.)) ;
#15357=CARTESIAN_POINT('',(0.,0.,0.)) ;
#15358=CARTESIAN_POINT('Origin',(0.,0.,0.4)) ;
#15359=CARTESIAN_POINT('',(-0.15,-1.83697019872103E-17,0.8)) ;
#15360=CARTESIAN_POINT('Origin',(0.,0.,0.8)) ;
#15361=CARTESIAN_POINT('',(-0.15,-1.83697019872103E-17,0.)) ;
#15362=CARTESIAN_POINT('',(-0.15,-1.83697019872103E-17,0.4)) ;
#15363=CARTESIAN_POINT('Origin',(0.,0.,0.)) ;
#15364=CARTESIAN_POINT('Origin',(0.,0.,0.8)) ;
#15365=CARTESIAN_POINT('Origin',(0.,0.,-0.1)) ;
#15366=CARTESIAN_POINT('',(-0.275,-3.36777869765522E-17,0.)) ;
#15367=CARTESIAN_POINT('Origin',(0.,0.,0.)) ;
#15368=CARTESIAN_POINT('',(-0.275,-3.36777869765522E-17,-0.2)) ;
#15369=CARTESIAN_POINT('',(-0.275,-3.36777869765522E-17,-0.1)) ;
#15370=CARTESIAN_POINT('Origin',(0.,0.,-0.2)) ;
#15371=CARTESIAN_POINT('Origin',(0.,0.,-0.2)) ;
#15372=CARTESIAN_POINT('Origin',(0.,0.,0.)) ;
#15439=UNCERTAINTY_MEASURE_WITH_UNIT(LENGTH_MEASURE(0.001),#15485,
'DISTANCE_ACCURACY_VALUE',
'Maximum model space distance between geometric entities at asserted c
onnectivities') ;
#15441=UNCERTAINTY_MEASURE_WITH_UNIT(LENGTH_MEASURE(0.001),#15485,
'DISTANCE_ACCURACY_VALUE',
'Maximum model space distance between geometric entities at asserted c
onnectivities') ;
#15482=(
GEOMETRIC_REPRESENTATION_CONTEXT(3)
GLOBAL_UNCERTAINTY_ASSIGNED_CONTEXT((#15439))
GLOBAL_UNIT_ASSIGNED_CONTEXT((#15485,#15487,#15488))
REPRESENTATION_CONTEXT('','3D')
) ;
#15484=(
GEOMETRIC_REPRESENTATION_CONTEXT(3)
GLOBAL_UNCERTAINTY_ASSIGNED_CONTEXT((#15441))
GLOBAL_UNIT_ASSIGNED_CONTEXT((#15485,#15487,#15488))
REPRESENTATION_CONTEXT('','3D')
) ;
#15485=(
LENGTH_UNIT()
NAMED_UNIT(*)
SI_UNIT(.CENTI.,.METRE.)
) ;
#15487=(
NAMED_UNIT(*)
PLANE_ANGLE_UNIT()
SI_UNIT($,.RADIAN.)
) ;
#15488=(
NAMED_UNIT(*)
SI_UNIT($,.STERADIAN.)
SOLID_ANGLE_UNIT()
) ;
#15529=SHAPE_DEFINITION_REPRESENTATION(#15606,#15658) ;
#15606=PRODUCT_DEFINITION_SHAPE('',$,#15701) ;
#15658=SHAPE_REPRESENTATION('',(#9895),#15482) ;
#15660=PRODUCT_DEFINITION_CONTEXT('part definition',#15788,'design') ;
#15701=PRODUCT_DEFINITION('RETAINER_SCREW_M3x8',
'RETAINER_SCREW_M3x8',#15743,#15660) ;
#15743=PRODUCT_DEFINITION_FORMATION('',$,#15830) ;
#15788=APPLICATION_CONTEXT(
'Core Data for Automotive Mechanical Design Process') ;
#15789=PRODUCT_CONTEXT('part definition',#15788,'mechanical') ;
#15830=PRODUCT('RETAINER_SCREW_M3x8','RETAINER_SCREW_M3x8',$,(#15789)) ;
#15832=PRESENTATION_STYLE_ASSIGNMENT((#15844)) ;
#15844=SURFACE_STYLE_USAGE(.BOTH.,#15856) ;
#15856=SURFACE_SIDE_STYLE('',(#15868)) ;
#15868=SURFACE_STYLE_FILL_AREA(#15880) ;
#15880=FILL_AREA_STYLE('Steel - Satin',(#15892)) ;
#15892=FILL_AREA_STYLE_COLOUR('Steel - Satin',#15904) ;
#15904=COLOUR_RGB('Steel - Satin', 0.72549020, 0.75294118, 0.79215686) ;
ENDSEC;
END-ISO-10303-21;
